ISO-10303-21;
HEADER;
/* Generated by software containing ST-Developer
 * from STEP Tools, Inc. (www.steptools.com) 
 */

FILE_DESCRIPTION(
/* description */ ('STEP AP214'),
/* implementation_level */ '2;1');

FILE_NAME(
/* name */ 'PRT-TQ-1012-11.step',
/* time_stamp */ '2026-10-07T12:49:37-07:00',
/* author */ (''),
/* organization */ (''),
/* preprocessor_version */ 'ST-DEVELOPER v20.2',
/* originating_system */ 'Autodesk Translation Framework v15.15.0.0',
/* authorisation */ '');

FILE_SCHEMA (('AUTOMOTIVE_DESIGN { 1 0 10303 214 3 1 1 }'));
ENDSEC;

DATA;
#10=MECHANICAL_DESIGN_GEOMETRIC_PRESENTATION_REPRESENTATION('',(#311),#33016);
#253=SHAPE_REPRESENTATION_RELATIONSHIP('SRR','None',#33148,#280);
#280=ADVANCED_BREP_SHAPE_REPRESENTATION('',(#338),#33009);
#311=STYLED_ITEM('',(#33288),#338);
#338=MANIFOLD_SOLID_BREP('Body1',#9962);
#363=CONICAL_SURFACE('',#11098,6.50000000000001,1.0471975511966);
#364=CONICAL_SURFACE('',#11101,13.8985,0.785398163397456);
#403=TOROIDAL_SURFACE('',#11099,14.5,0.5);
#543=FACE_BOUND('',#2116,.T.);
#544=FACE_BOUND('',#2118,.T.);
#545=FACE_BOUND('',#2128,.T.);
#975=PLANE('',#11060);
#976=PLANE('',#11063);
#977=PLANE('',#11065);
#978=PLANE('',#11066);
#979=PLANE('',#11067);
#980=PLANE('',#11068);
#981=PLANE('',#11069);
#982=PLANE('',#11070);
#983=PLANE('',#11078);
#984=PLANE('',#11080);
#985=PLANE('',#11081);
#986=PLANE('',#11082);
#987=PLANE('',#11083);
#988=PLANE('',#11084);
#989=PLANE('',#11085);
#990=PLANE('',#11086);
#991=PLANE('',#11087);
#992=PLANE('',#11088);
#993=PLANE('',#11089);
#994=PLANE('',#11090);
#995=PLANE('',#11091);
#996=PLANE('',#11092);
#997=PLANE('',#11093);
#998=PLANE('',#11094);
#999=PLANE('',#11095);
#1000=PLANE('',#11096);
#1001=PLANE('',#11097);
#1490=FACE_OUTER_BOUND('',#2115,.T.);
#1491=FACE_OUTER_BOUND('',#2117,.T.);
#1492=FACE_OUTER_BOUND('',#2119,.T.);
#1493=FACE_OUTER_BOUND('',#2120,.T.);
#1494=FACE_OUTER_BOUND('',#2121,.T.);
#1495=FACE_OUTER_BOUND('',#2122,.T.);
#1496=FACE_OUTER_BOUND('',#2123,.T.);
#1497=FACE_OUTER_BOUND('',#2124,.T.);
#1498=FACE_OUTER_BOUND('',#2125,.T.);
#1499=FACE_OUTER_BOUND('',#2126,.T.);
#1500=FACE_OUTER_BOUND('',#2127,.T.);
#1501=FACE_OUTER_BOUND('',#2129,.T.);
#1502=FACE_OUTER_BOUND('',#2130,.T.);
#1503=FACE_OUTER_BOUND('',#2131,.T.);
#1504=FACE_OUTER_BOUND('',#2132,.T.);
#1505=FACE_OUTER_BOUND('',#2133,.T.);
#1506=FACE_OUTER_BOUND('',#2134,.T.);
#1507=FACE_OUTER_BOUND('',#2135,.T.);
#1508=FACE_OUTER_BOUND('',#2136,.T.);
#1509=FACE_OUTER_BOUND('',#2137,.T.);
#1510=FACE_OUTER_BOUND('',#2138,.T.);
#1511=FACE_OUTER_BOUND('',#2139,.T.);
#1512=FACE_OUTER_BOUND('',#2140,.T.);
#1513=FACE_OUTER_BOUND('',#2141,.T.);
#1514=FACE_OUTER_BOUND('',#2142,.T.);
#1515=FACE_OUTER_BOUND('',#2143,.T.);
#1516=FACE_OUTER_BOUND('',#2144,.T.);
#1517=FACE_OUTER_BOUND('',#2145,.T.);
#1518=FACE_OUTER_BOUND('',#2146,.T.);
#1519=FACE_OUTER_BOUND('',#2147,.T.);
#1520=FACE_OUTER_BOUND('',#2148,.T.);
#1521=FACE_OUTER_BOUND('',#2149,.T.);
#2115=EDGE_LOOP('',(#8808));
#2116=EDGE_LOOP('',(#8809));
#2117=EDGE_LOOP('',(#8810));
#2118=EDGE_LOOP('',(#8811,#8812,#8813,#8814,#8815,#8816,#8817,#8818,#8819,
#8820,#8821,#8822,#8823,#8824,#8825,#8826,#8827,#8828,#8829,#8830,#8831,
#8832,#8833,#8834));
#2119=EDGE_LOOP('',(#8835,#8836,#8837,#8838));
#2120=EDGE_LOOP('',(#8839,#8840,#8841,#8842));
#2121=EDGE_LOOP('',(#8843,#8844,#8845,#8846));
#2122=EDGE_LOOP('',(#8847,#8848,#8849,#8850));
#2123=EDGE_LOOP('',(#8851,#8852,#8853,#8854));
#2124=EDGE_LOOP('',(#8855,#8856,#8857,#8858));
#2125=EDGE_LOOP('',(#8859,#8860,#8861,#8862,#8863));
#2126=EDGE_LOOP('',(#8864,#8865,#8866,#8867,#8868));
#2127=EDGE_LOOP('',(#8869,#8870,#8871,#8872,#8873,#8874,#8875,#8876,#8877,
#8878,#8879,#8880,#8881,#8882,#8883,#8884,#8885,#8886,#8887,#8888,#8889,
#8890,#8891,#8892));
#2128=EDGE_LOOP('',(#8893));
#2129=EDGE_LOOP('',(#8894,#8895,#8896,#8897));
#2130=EDGE_LOOP('',(#8898,#8899,#8900,#8901));
#2131=EDGE_LOOP('',(#8902,#8903,#8904,#8905));
#2132=EDGE_LOOP('',(#8906,#8907,#8908,#8909));
#2133=EDGE_LOOP('',(#8910,#8911,#8912,#8913));
#2134=EDGE_LOOP('',(#8914,#8915,#8916,#8917));
#2135=EDGE_LOOP('',(#8918,#8919,#8920,#8921));
#2136=EDGE_LOOP('',(#8922,#8923,#8924,#8925));
#2137=EDGE_LOOP('',(#8926,#8927,#8928,#8929));
#2138=EDGE_LOOP('',(#8930,#8931,#8932,#8933));
#2139=EDGE_LOOP('',(#8934,#8935,#8936,#8937));
#2140=EDGE_LOOP('',(#8938,#8939,#8940,#8941));
#2141=EDGE_LOOP('',(#8942,#8943,#8944,#8945));
#2142=EDGE_LOOP('',(#8946,#8947,#8948,#8949));
#2143=EDGE_LOOP('',(#8950,#8951,#8952,#8953));
#2144=EDGE_LOOP('',(#8954,#8955,#8956,#8957));
#2145=EDGE_LOOP('',(#8958,#8959,#8960,#8961));
#2146=EDGE_LOOP('',(#8962,#8963,#8964,#8965));
#2147=EDGE_LOOP('',(#8966,#8967,#8968,#8969,#8970));
#2148=EDGE_LOOP('',(#8971,#8972,#8973,#8974,#8975));
#2149=EDGE_LOOP('',(#8976,#8977,#8978,#8979));
#2534=CIRCLE('',#11061,13.8985);
#2535=CIRCLE('',#11062,4.5);
#2536=CIRCLE('',#11064,14.5);
#2537=CIRCLE('',#11072,4.5);
#2538=CIRCLE('',#11073,4.5);
#2539=CIRCLE('',#11075,15.);
#2540=CIRCLE('',#11076,15.);
#2541=CIRCLE('',#11077,15.);
#2542=CIRCLE('',#11079,6.50000000000001);
#2543=CIRCLE('',#11100,0.5);
#3239=LINE('',#31169,#3989);
#3240=LINE('',#31171,#3990);
#3241=LINE('',#31173,#3991);
#3242=LINE('',#31175,#3992);
#3243=LINE('',#31177,#3993);
#3244=LINE('',#31179,#3994);
#3245=LINE('',#31181,#3995);
#3246=LINE('',#31183,#3996);
#3247=LINE('',#31185,#3997);
#3248=LINE('',#31187,#3998);
#3249=LINE('',#31189,#3999);
#3250=LINE('',#31191,#4000);
#3251=LINE('',#31193,#4001);
#3252=LINE('',#31195,#4002);
#3253=LINE('',#31197,#4003);
#3254=LINE('',#31199,#4004);
#3255=LINE('',#31201,#4005);
#3256=LINE('',#31203,#4006);
#3257=LINE('',#31205,#4007);
#3258=LINE('',#31207,#4008);
#3259=LINE('',#31209,#4009);
#3260=LINE('',#31211,#4010);
#3261=LINE('',#31213,#4011);
#3262=LINE('',#31214,#4012);
#3263=LINE('',#31218,#4013);
#3264=LINE('',#31219,#4014);
#3265=LINE('',#31220,#4015);
#3266=LINE('',#31224,#4016);
#3267=LINE('',#31225,#4017);
#3268=LINE('',#31226,#4018);
#3269=LINE('',#31230,#4019);
#3270=LINE('',#31231,#4020);
#3271=LINE('',#31232,#4021);
#3272=LINE('',#31235,#4022);
#3273=LINE('',#31237,#4023);
#3274=LINE('',#31238,#4024);
#3275=LINE('',#31241,#4025);
#3276=LINE('',#31242,#4026);
#3277=LINE('',#31246,#4027);
#3278=LINE('',#31247,#4028);
#3279=LINE('',#31248,#4029);
#3280=LINE('',#31254,#4030);
#3281=LINE('',#31261,#4031);
#3282=LINE('',#31266,#4032);
#3283=LINE('',#31268,#4033);
#3284=LINE('',#31269,#4034);
#3285=LINE('',#31271,#4035);
#3286=LINE('',#31273,#4036);
#3287=LINE('',#31274,#4037);
#3288=LINE('',#31276,#4038);
#3289=LINE('',#31278,#4039);
#3290=LINE('',#31279,#4040);
#3291=LINE('',#31281,#4041);
#3292=LINE('',#31283,#4042);
#3293=LINE('',#31284,#4043);
#3294=LINE('',#31286,#4044);
#3295=LINE('',#31288,#4045);
#3296=LINE('',#31289,#4046);
#3297=LINE('',#31291,#4047);
#3298=LINE('',#31293,#4048);
#3299=LINE('',#31294,#4049);
#3300=LINE('',#31298,#4050);
#3301=LINE('',#31300,#4051);
#3302=LINE('',#31302,#4052);
#3303=LINE('',#31303,#4053);
#3304=LINE('',#31305,#4054);
#3305=LINE('',#31307,#4055);
#3306=LINE('',#31309,#4056);
#3307=LINE('',#31311,#4057);
#3308=LINE('',#31314,#4058);
#3309=LINE('',#31317,#4059);
#3310=LINE('',#31320,#4060);
#3311=LINE('',#31323,#4061);
#3312=LINE('',#31326,#4062);
#3313=LINE('',#31329,#4063);
#3314=LINE('',#31333,#4064);
#3989=VECTOR('',#13468,1000.);
#3990=VECTOR('',#13469,1000.);
#3991=VECTOR('',#13470,1000.);
#3992=VECTOR('',#13471,1000.);
#3993=VECTOR('',#13472,1000.);
#3994=VECTOR('',#13473,1000.);
#3995=VECTOR('',#13474,1000.);
#3996=VECTOR('',#13475,1000.);
#3997=VECTOR('',#13476,1000.);
#3998=VECTOR('',#13477,1000.);
#3999=VECTOR('',#13478,1000.);
#4000=VECTOR('',#13479,1000.);
#4001=VECTOR('',#13480,1000.);
#4002=VECTOR('',#13481,1000.);
#4003=VECTOR('',#13482,1000.);
#4004=VECTOR('',#13483,1000.);
#4005=VECTOR('',#13484,1000.);
#4006=VECTOR('',#13485,1000.);
#4007=VECTOR('',#13486,1000.);
#4008=VECTOR('',#13487,1000.);
#4009=VECTOR('',#13488,1000.);
#4010=VECTOR('',#13489,1000.);
#4011=VECTOR('',#13490,1000.);
#4012=VECTOR('',#13491,1000.);
#4013=VECTOR('',#13494,1000.);
#4014=VECTOR('',#13495,1000.);
#4015=VECTOR('',#13496,1000.);
#4016=VECTOR('',#13499,1000.);
#4017=VECTOR('',#13500,1000.);
#4018=VECTOR('',#13501,1000.);
#4019=VECTOR('',#13504,1000.);
#4020=VECTOR('',#13505,1000.);
#4021=VECTOR('',#13506,1000.);
#4022=VECTOR('',#13509,1000.);
#4023=VECTOR('',#13510,1000.);
#4024=VECTOR('',#13511,1000.);
#4025=VECTOR('',#13514,1000.);
#4026=VECTOR('',#13515,1000.);
#4027=VECTOR('',#13518,1000.);
#4028=VECTOR('',#13519,1000.);
#4029=VECTOR('',#13520,1000.);
#4030=VECTOR('',#13527,4.5);
#4031=VECTOR('',#13534,15.);
#4032=VECTOR('',#13539,1000.);
#4033=VECTOR('',#13540,1000.);
#4034=VECTOR('',#13541,1000.);
#4035=VECTOR('',#13542,1000.);
#4036=VECTOR('',#13543,1000.);
#4037=VECTOR('',#13544,1000.);
#4038=VECTOR('',#13545,1000.);
#4039=VECTOR('',#13546,1000.);
#4040=VECTOR('',#13547,1000.);
#4041=VECTOR('',#13548,1000.);
#4042=VECTOR('',#13549,1000.);
#4043=VECTOR('',#13550,1000.);
#4044=VECTOR('',#13551,1000.);
#4045=VECTOR('',#13552,1000.);
#4046=VECTOR('',#13553,1000.);
#4047=VECTOR('',#13554,1000.);
#4048=VECTOR('',#13555,1000.);
#4049=VECTOR('',#13556,1000.);
#4050=VECTOR('',#13561,1000.);
#4051=VECTOR('',#13564,1000.);
#4052=VECTOR('',#13567,1000.);
#4053=VECTOR('',#13568,1000.);
#4054=VECTOR('',#13571,1000.);
#4055=VECTOR('',#13574,1000.);
#4056=VECTOR('',#13577,1000.);
#4057=VECTOR('',#13580,1000.);
#4058=VECTOR('',#13585,1000.);
#4059=VECTOR('',#13590,1000.);
#4060=VECTOR('',#13595,1000.);
#4061=VECTOR('',#13600,1000.);
#4062=VECTOR('',#13605,1000.);
#4063=VECTOR('',#13610,6.50000000000001);
#4064=VECTOR('',#13617,13.8985);
#4889=VERTEX_POINT('',#31160);
#4890=VERTEX_POINT('',#31162);
#4891=VERTEX_POINT('',#31165);
#4892=VERTEX_POINT('',#31167);
#4893=VERTEX_POINT('',#31168);
#4894=VERTEX_POINT('',#31170);
#4895=VERTEX_POINT('',#31172);
#4896=VERTEX_POINT('',#31174);
#4897=VERTEX_POINT('',#31176);
#4898=VERTEX_POINT('',#31178);
#4899=VERTEX_POINT('',#31180);
#4900=VERTEX_POINT('',#31182);
#4901=VERTEX_POINT('',#31184);
#4902=VERTEX_POINT('',#31186);
#4903=VERTEX_POINT('',#31188);
#4904=VERTEX_POINT('',#31190);
#4905=VERTEX_POINT('',#31192);
#4906=VERTEX_POINT('',#31194);
#4907=VERTEX_POINT('',#31196);
#4908=VERTEX_POINT('',#31198);
#4909=VERTEX_POINT('',#31200);
#4910=VERTEX_POINT('',#31202);
#4911=VERTEX_POINT('',#31204);
#4912=VERTEX_POINT('',#31206);
#4913=VERTEX_POINT('',#31208);
#4914=VERTEX_POINT('',#31210);
#4915=VERTEX_POINT('',#31212);
#4916=VERTEX_POINT('',#31216);
#4917=VERTEX_POINT('',#31217);
#4918=VERTEX_POINT('',#31222);
#4919=VERTEX_POINT('',#31223);
#4920=VERTEX_POINT('',#31228);
#4921=VERTEX_POINT('',#31229);
#4922=VERTEX_POINT('',#31234);
#4923=VERTEX_POINT('',#31236);
#4924=VERTEX_POINT('',#31240);
#4925=VERTEX_POINT('',#31244);
#4926=VERTEX_POINT('',#31245);
#4927=VERTEX_POINT('',#31250);
#4928=VERTEX_POINT('',#31251);
#4929=VERTEX_POINT('',#31256);
#4930=VERTEX_POINT('',#31257);
#4931=VERTEX_POINT('',#31260);
#4932=VERTEX_POINT('',#31264);
#4933=VERTEX_POINT('',#31265);
#4934=VERTEX_POINT('',#31267);
#4935=VERTEX_POINT('',#31270);
#4936=VERTEX_POINT('',#31272);
#4937=VERTEX_POINT('',#31275);
#4938=VERTEX_POINT('',#31277);
#4939=VERTEX_POINT('',#31280);
#4940=VERTEX_POINT('',#31282);
#4941=VERTEX_POINT('',#31285);
#4942=VERTEX_POINT('',#31287);
#4943=VERTEX_POINT('',#31290);
#4944=VERTEX_POINT('',#31292);
#4945=VERTEX_POINT('',#31295);
#6217=EDGE_CURVE('',#4889,#4889,#2534,.T.);
#6218=EDGE_CURVE('',#4890,#4890,#2535,.T.);
#6219=EDGE_CURVE('',#4891,#4891,#2536,.T.);
#6220=EDGE_CURVE('',#4892,#4893,#3239,.T.);
#6221=EDGE_CURVE('',#4894,#4892,#3240,.T.);
#6222=EDGE_CURVE('',#4895,#4894,#3241,.T.);
#6223=EDGE_CURVE('',#4896,#4895,#3242,.T.);
#6224=EDGE_CURVE('',#4897,#4896,#3243,.T.);
#6225=EDGE_CURVE('',#4898,#4897,#3244,.T.);
#6226=EDGE_CURVE('',#4899,#4898,#3245,.T.);
#6227=EDGE_CURVE('',#4900,#4899,#3246,.T.);
#6228=EDGE_CURVE('',#4901,#4900,#3247,.T.);
#6229=EDGE_CURVE('',#4902,#4901,#3248,.T.);
#6230=EDGE_CURVE('',#4903,#4902,#3249,.T.);
#6231=EDGE_CURVE('',#4904,#4903,#3250,.T.);
#6232=EDGE_CURVE('',#4905,#4904,#3251,.T.);
#6233=EDGE_CURVE('',#4906,#4905,#3252,.T.);
#6234=EDGE_CURVE('',#4907,#4906,#3253,.T.);
#6235=EDGE_CURVE('',#4908,#4907,#3254,.T.);
#6236=EDGE_CURVE('',#4909,#4908,#3255,.T.);
#6237=EDGE_CURVE('',#4910,#4909,#3256,.T.);
#6238=EDGE_CURVE('',#4911,#4910,#3257,.T.);
#6239=EDGE_CURVE('',#4912,#4911,#3258,.T.);
#6240=EDGE_CURVE('',#4913,#4912,#3259,.T.);
#6241=EDGE_CURVE('',#4914,#4913,#3260,.T.);
#6242=EDGE_CURVE('',#4915,#4914,#3261,.T.);
#6243=EDGE_CURVE('',#4893,#4915,#3262,.T.);
#6244=EDGE_CURVE('',#4916,#4917,#3263,.T.);
#6245=EDGE_CURVE('',#4916,#4903,#3264,.T.);
#6246=EDGE_CURVE('',#4917,#4902,#3265,.T.);
#6247=EDGE_CURVE('',#4918,#4919,#3266,.T.);
#6248=EDGE_CURVE('',#4918,#4907,#3267,.T.);
#6249=EDGE_CURVE('',#4919,#4906,#3268,.T.);
#6250=EDGE_CURVE('',#4920,#4921,#3269,.T.);
#6251=EDGE_CURVE('',#4920,#4911,#3270,.T.);
#6252=EDGE_CURVE('',#4921,#4910,#3271,.T.);
#6253=EDGE_CURVE('',#4892,#4922,#3272,.T.);
#6254=EDGE_CURVE('',#4923,#4922,#3273,.T.);
#6255=EDGE_CURVE('',#4923,#4894,#3274,.T.);
#6256=EDGE_CURVE('',#4924,#4923,#3275,.T.);
#6257=EDGE_CURVE('',#4924,#4895,#3276,.T.);
#6258=EDGE_CURVE('',#4925,#4926,#3277,.T.);
#6259=EDGE_CURVE('',#4925,#4899,#3278,.T.);
#6260=EDGE_CURVE('',#4926,#4898,#3279,.T.);
#6261=EDGE_CURVE('',#4927,#4928,#2537,.T.);
#6262=EDGE_CURVE('',#4928,#4927,#2538,.T.);
#6263=EDGE_CURVE('',#4927,#4890,#3280,.T.);
#6264=EDGE_CURVE('',#4929,#4930,#2539,.T.);
#6265=EDGE_CURVE('',#4930,#4929,#2540,.T.);
#6266=EDGE_CURVE('',#4929,#4931,#3281,.T.);
#6267=EDGE_CURVE('',#4931,#4931,#2541,.T.);
#6268=EDGE_CURVE('',#4932,#4933,#3282,.T.);
#6269=EDGE_CURVE('',#4933,#4934,#3283,.T.);
#6270=EDGE_CURVE('',#4934,#4920,#3284,.T.);
#6271=EDGE_CURVE('',#4921,#4935,#3285,.T.);
#6272=EDGE_CURVE('',#4935,#4936,#3286,.T.);
#6273=EDGE_CURVE('',#4936,#4918,#3287,.T.);
#6274=EDGE_CURVE('',#4919,#4937,#3288,.T.);
#6275=EDGE_CURVE('',#4937,#4938,#3289,.T.);
#6276=EDGE_CURVE('',#4938,#4916,#3290,.T.);
#6277=EDGE_CURVE('',#4917,#4939,#3291,.T.);
#6278=EDGE_CURVE('',#4939,#4940,#3292,.T.);
#6279=EDGE_CURVE('',#4940,#4925,#3293,.T.);
#6280=EDGE_CURVE('',#4926,#4941,#3294,.T.);
#6281=EDGE_CURVE('',#4941,#4942,#3295,.T.);
#6282=EDGE_CURVE('',#4942,#4924,#3296,.T.);
#6283=EDGE_CURVE('',#4922,#4943,#3297,.T.);
#6284=EDGE_CURVE('',#4943,#4944,#3298,.T.);
#6285=EDGE_CURVE('',#4944,#4932,#3299,.T.);
#6286=EDGE_CURVE('',#4945,#4945,#2542,.T.);
#6287=EDGE_CURVE('',#4905,#4937,#3300,.T.);
#6288=EDGE_CURVE('',#4909,#4935,#3301,.T.);
#6289=EDGE_CURVE('',#4913,#4933,#3302,.T.);
#6290=EDGE_CURVE('',#4932,#4914,#3303,.T.);
#6291=EDGE_CURVE('',#4944,#4915,#3304,.T.);
#6292=EDGE_CURVE('',#4897,#4941,#3305,.T.);
#6293=EDGE_CURVE('',#4901,#4939,#3306,.T.);
#6294=EDGE_CURVE('',#4940,#4900,#3307,.T.);
#6295=EDGE_CURVE('',#4942,#4896,#3308,.T.);
#6296=EDGE_CURVE('',#4943,#4893,#3309,.T.);
#6297=EDGE_CURVE('',#4934,#4912,#3310,.T.);
#6298=EDGE_CURVE('',#4936,#4908,#3311,.T.);
#6299=EDGE_CURVE('',#4938,#4904,#3312,.T.);
#6300=EDGE_CURVE('',#4928,#4945,#3313,.T.);
#6301=EDGE_CURVE('',#4930,#4891,#2543,.T.);
#6302=EDGE_CURVE('',#4931,#4889,#3314,.T.);
#8808=ORIENTED_EDGE('',*,*,#6217,.F.);
#8809=ORIENTED_EDGE('',*,*,#6218,.F.);
#8810=ORIENTED_EDGE('',*,*,#6219,.T.);
#8811=ORIENTED_EDGE('',*,*,#6220,.F.);
#8812=ORIENTED_EDGE('',*,*,#6221,.F.);
#8813=ORIENTED_EDGE('',*,*,#6222,.F.);
#8814=ORIENTED_EDGE('',*,*,#6223,.F.);
#8815=ORIENTED_EDGE('',*,*,#6224,.F.);
#8816=ORIENTED_EDGE('',*,*,#6225,.F.);
#8817=ORIENTED_EDGE('',*,*,#6226,.F.);
#8818=ORIENTED_EDGE('',*,*,#6227,.F.);
#8819=ORIENTED_EDGE('',*,*,#6228,.F.);
#8820=ORIENTED_EDGE('',*,*,#6229,.F.);
#8821=ORIENTED_EDGE('',*,*,#6230,.F.);
#8822=ORIENTED_EDGE('',*,*,#6231,.F.);
#8823=ORIENTED_EDGE('',*,*,#6232,.F.);
#8824=ORIENTED_EDGE('',*,*,#6233,.F.);
#8825=ORIENTED_EDGE('',*,*,#6234,.F.);
#8826=ORIENTED_EDGE('',*,*,#6235,.F.);
#8827=ORIENTED_EDGE('',*,*,#6236,.F.);
#8828=ORIENTED_EDGE('',*,*,#6237,.F.);
#8829=ORIENTED_EDGE('',*,*,#6238,.F.);
#8830=ORIENTED_EDGE('',*,*,#6239,.F.);
#8831=ORIENTED_EDGE('',*,*,#6240,.F.);
#8832=ORIENTED_EDGE('',*,*,#6241,.F.);
#8833=ORIENTED_EDGE('',*,*,#6242,.F.);
#8834=ORIENTED_EDGE('',*,*,#6243,.F.);
#8835=ORIENTED_EDGE('',*,*,#6244,.F.);
#8836=ORIENTED_EDGE('',*,*,#6245,.T.);
#8837=ORIENTED_EDGE('',*,*,#6230,.T.);
#8838=ORIENTED_EDGE('',*,*,#6246,.F.);
#8839=ORIENTED_EDGE('',*,*,#6247,.F.);
#8840=ORIENTED_EDGE('',*,*,#6248,.T.);
#8841=ORIENTED_EDGE('',*,*,#6234,.T.);
#8842=ORIENTED_EDGE('',*,*,#6249,.F.);
#8843=ORIENTED_EDGE('',*,*,#6250,.F.);
#8844=ORIENTED_EDGE('',*,*,#6251,.T.);
#8845=ORIENTED_EDGE('',*,*,#6238,.T.);
#8846=ORIENTED_EDGE('',*,*,#6252,.F.);
#8847=ORIENTED_EDGE('',*,*,#6221,.T.);
#8848=ORIENTED_EDGE('',*,*,#6253,.T.);
#8849=ORIENTED_EDGE('',*,*,#6254,.F.);
#8850=ORIENTED_EDGE('',*,*,#6255,.T.);
#8851=ORIENTED_EDGE('',*,*,#6256,.F.);
#8852=ORIENTED_EDGE('',*,*,#6257,.T.);
#8853=ORIENTED_EDGE('',*,*,#6222,.T.);
#8854=ORIENTED_EDGE('',*,*,#6255,.F.);
#8855=ORIENTED_EDGE('',*,*,#6258,.F.);
#8856=ORIENTED_EDGE('',*,*,#6259,.T.);
#8857=ORIENTED_EDGE('',*,*,#6226,.T.);
#8858=ORIENTED_EDGE('',*,*,#6260,.F.);
#8859=ORIENTED_EDGE('',*,*,#6261,.T.);
#8860=ORIENTED_EDGE('',*,*,#6262,.T.);
#8861=ORIENTED_EDGE('',*,*,#6263,.T.);
#8862=ORIENTED_EDGE('',*,*,#6218,.T.);
#8863=ORIENTED_EDGE('',*,*,#6263,.F.);
#8864=ORIENTED_EDGE('',*,*,#6264,.T.);
#8865=ORIENTED_EDGE('',*,*,#6265,.T.);
#8866=ORIENTED_EDGE('',*,*,#6266,.T.);
#8867=ORIENTED_EDGE('',*,*,#6267,.T.);
#8868=ORIENTED_EDGE('',*,*,#6266,.F.);
#8869=ORIENTED_EDGE('',*,*,#6268,.T.);
#8870=ORIENTED_EDGE('',*,*,#6269,.T.);
#8871=ORIENTED_EDGE('',*,*,#6270,.T.);
#8872=ORIENTED_EDGE('',*,*,#6250,.T.);
#8873=ORIENTED_EDGE('',*,*,#6271,.T.);
#8874=ORIENTED_EDGE('',*,*,#6272,.T.);
#8875=ORIENTED_EDGE('',*,*,#6273,.T.);
#8876=ORIENTED_EDGE('',*,*,#6247,.T.);
#8877=ORIENTED_EDGE('',*,*,#6274,.T.);
#8878=ORIENTED_EDGE('',*,*,#6275,.T.);
#8879=ORIENTED_EDGE('',*,*,#6276,.T.);
#8880=ORIENTED_EDGE('',*,*,#6244,.T.);
#8881=ORIENTED_EDGE('',*,*,#6277,.T.);
#8882=ORIENTED_EDGE('',*,*,#6278,.T.);
#8883=ORIENTED_EDGE('',*,*,#6279,.T.);
#8884=ORIENTED_EDGE('',*,*,#6258,.T.);
#8885=ORIENTED_EDGE('',*,*,#6280,.T.);
#8886=ORIENTED_EDGE('',*,*,#6281,.T.);
#8887=ORIENTED_EDGE('',*,*,#6282,.T.);
#8888=ORIENTED_EDGE('',*,*,#6256,.T.);
#8889=ORIENTED_EDGE('',*,*,#6254,.T.);
#8890=ORIENTED_EDGE('',*,*,#6283,.T.);
#8891=ORIENTED_EDGE('',*,*,#6284,.T.);
#8892=ORIENTED_EDGE('',*,*,#6285,.T.);
#8893=ORIENTED_EDGE('',*,*,#6286,.T.);
#8894=ORIENTED_EDGE('',*,*,#6233,.T.);
#8895=ORIENTED_EDGE('',*,*,#6287,.T.);
#8896=ORIENTED_EDGE('',*,*,#6274,.F.);
#8897=ORIENTED_EDGE('',*,*,#6249,.T.);
#8898=ORIENTED_EDGE('',*,*,#6237,.T.);
#8899=ORIENTED_EDGE('',*,*,#6288,.T.);
#8900=ORIENTED_EDGE('',*,*,#6271,.F.);
#8901=ORIENTED_EDGE('',*,*,#6252,.T.);
#8902=ORIENTED_EDGE('',*,*,#6241,.T.);
#8903=ORIENTED_EDGE('',*,*,#6289,.T.);
#8904=ORIENTED_EDGE('',*,*,#6268,.F.);
#8905=ORIENTED_EDGE('',*,*,#6290,.T.);
#8906=ORIENTED_EDGE('',*,*,#6285,.F.);
#8907=ORIENTED_EDGE('',*,*,#6291,.T.);
#8908=ORIENTED_EDGE('',*,*,#6242,.T.);
#8909=ORIENTED_EDGE('',*,*,#6290,.F.);
#8910=ORIENTED_EDGE('',*,*,#6225,.T.);
#8911=ORIENTED_EDGE('',*,*,#6292,.T.);
#8912=ORIENTED_EDGE('',*,*,#6280,.F.);
#8913=ORIENTED_EDGE('',*,*,#6260,.T.);
#8914=ORIENTED_EDGE('',*,*,#6229,.T.);
#8915=ORIENTED_EDGE('',*,*,#6293,.T.);
#8916=ORIENTED_EDGE('',*,*,#6277,.F.);
#8917=ORIENTED_EDGE('',*,*,#6246,.T.);
#8918=ORIENTED_EDGE('',*,*,#6228,.T.);
#8919=ORIENTED_EDGE('',*,*,#6294,.F.);
#8920=ORIENTED_EDGE('',*,*,#6278,.F.);
#8921=ORIENTED_EDGE('',*,*,#6293,.F.);
#8922=ORIENTED_EDGE('',*,*,#6279,.F.);
#8923=ORIENTED_EDGE('',*,*,#6294,.T.);
#8924=ORIENTED_EDGE('',*,*,#6227,.T.);
#8925=ORIENTED_EDGE('',*,*,#6259,.F.);
#8926=ORIENTED_EDGE('',*,*,#6224,.T.);
#8927=ORIENTED_EDGE('',*,*,#6295,.F.);
#8928=ORIENTED_EDGE('',*,*,#6281,.F.);
#8929=ORIENTED_EDGE('',*,*,#6292,.F.);
#8930=ORIENTED_EDGE('',*,*,#6282,.F.);
#8931=ORIENTED_EDGE('',*,*,#6295,.T.);
#8932=ORIENTED_EDGE('',*,*,#6223,.T.);
#8933=ORIENTED_EDGE('',*,*,#6257,.F.);
#8934=ORIENTED_EDGE('',*,*,#6284,.F.);
#8935=ORIENTED_EDGE('',*,*,#6296,.T.);
#8936=ORIENTED_EDGE('',*,*,#6243,.T.);
#8937=ORIENTED_EDGE('',*,*,#6291,.F.);
#8938=ORIENTED_EDGE('',*,*,#6220,.T.);
#8939=ORIENTED_EDGE('',*,*,#6296,.F.);
#8940=ORIENTED_EDGE('',*,*,#6283,.F.);
#8941=ORIENTED_EDGE('',*,*,#6253,.F.);
#8942=ORIENTED_EDGE('',*,*,#6240,.T.);
#8943=ORIENTED_EDGE('',*,*,#6297,.F.);
#8944=ORIENTED_EDGE('',*,*,#6269,.F.);
#8945=ORIENTED_EDGE('',*,*,#6289,.F.);
#8946=ORIENTED_EDGE('',*,*,#6270,.F.);
#8947=ORIENTED_EDGE('',*,*,#6297,.T.);
#8948=ORIENTED_EDGE('',*,*,#6239,.T.);
#8949=ORIENTED_EDGE('',*,*,#6251,.F.);
#8950=ORIENTED_EDGE('',*,*,#6236,.T.);
#8951=ORIENTED_EDGE('',*,*,#6298,.F.);
#8952=ORIENTED_EDGE('',*,*,#6272,.F.);
#8953=ORIENTED_EDGE('',*,*,#6288,.F.);
#8954=ORIENTED_EDGE('',*,*,#6273,.F.);
#8955=ORIENTED_EDGE('',*,*,#6298,.T.);
#8956=ORIENTED_EDGE('',*,*,#6235,.T.);
#8957=ORIENTED_EDGE('',*,*,#6248,.F.);
#8958=ORIENTED_EDGE('',*,*,#6232,.T.);
#8959=ORIENTED_EDGE('',*,*,#6299,.F.);
#8960=ORIENTED_EDGE('',*,*,#6275,.F.);
#8961=ORIENTED_EDGE('',*,*,#6287,.F.);
#8962=ORIENTED_EDGE('',*,*,#6276,.F.);
#8963=ORIENTED_EDGE('',*,*,#6299,.T.);
#8964=ORIENTED_EDGE('',*,*,#6231,.T.);
#8965=ORIENTED_EDGE('',*,*,#6245,.F.);
#8966=ORIENTED_EDGE('',*,*,#6261,.F.);
#8967=ORIENTED_EDGE('',*,*,#6262,.F.);
#8968=ORIENTED_EDGE('',*,*,#6300,.T.);
#8969=ORIENTED_EDGE('',*,*,#6286,.F.);
#8970=ORIENTED_EDGE('',*,*,#6300,.F.);
#8971=ORIENTED_EDGE('',*,*,#6264,.F.);
#8972=ORIENTED_EDGE('',*,*,#6265,.F.);
#8973=ORIENTED_EDGE('',*,*,#6301,.T.);
#8974=ORIENTED_EDGE('',*,*,#6219,.F.);
#8975=ORIENTED_EDGE('',*,*,#6301,.F.);
#8976=ORIENTED_EDGE('',*,*,#6267,.F.);
#8977=ORIENTED_EDGE('',*,*,#6302,.T.);
#8978=ORIENTED_EDGE('',*,*,#6217,.T.);
#8979=ORIENTED_EDGE('',*,*,#6302,.F.);
#9374=CYLINDRICAL_SURFACE('',#11071,4.5);
#9375=CYLINDRICAL_SURFACE('',#11074,15.);
#9856=ADVANCED_FACE('',(#1490,#543),#975,.F.);
#9857=ADVANCED_FACE('',(#1491,#544),#976,.F.);
#9858=ADVANCED_FACE('',(#1492),#977,.F.);
#9859=ADVANCED_FACE('',(#1493),#978,.F.);
#9860=ADVANCED_FACE('',(#1494),#979,.F.);
#9861=ADVANCED_FACE('',(#1495),#980,.F.);
#9862=ADVANCED_FACE('',(#1496),#981,.F.);
#9863=ADVANCED_FACE('',(#1497),#982,.F.);
#9864=ADVANCED_FACE('',(#1498),#9374,.F.);
#9865=ADVANCED_FACE('',(#1499),#9375,.T.);
#9866=ADVANCED_FACE('',(#1500,#545),#983,.T.);
#9867=ADVANCED_FACE('',(#1501),#984,.F.);
#9868=ADVANCED_FACE('',(#1502),#985,.F.);
#9869=ADVANCED_FACE('',(#1503),#986,.F.);
#9870=ADVANCED_FACE('',(#1504),#987,.F.);
#9871=ADVANCED_FACE('',(#1505),#988,.F.);
#9872=ADVANCED_FACE('',(#1506),#989,.F.);
#9873=ADVANCED_FACE('',(#1507),#990,.F.);
#9874=ADVANCED_FACE('',(#1508),#991,.F.);
#9875=ADVANCED_FACE('',(#1509),#992,.F.);
#9876=ADVANCED_FACE('',(#1510),#993,.F.);
#9877=ADVANCED_FACE('',(#1511),#994,.F.);
#9878=ADVANCED_FACE('',(#1512),#995,.F.);
#9879=ADVANCED_FACE('',(#1513),#996,.F.);
#9880=ADVANCED_FACE('',(#1514),#997,.F.);
#9881=ADVANCED_FACE('',(#1515),#998,.F.);
#9882=ADVANCED_FACE('',(#1516),#999,.F.);
#9883=ADVANCED_FACE('',(#1517),#1000,.F.);
#9884=ADVANCED_FACE('',(#1518),#1001,.F.);
#9885=ADVANCED_FACE('',(#1519),#363,.F.);
#9886=ADVANCED_FACE('',(#1520),#403,.T.);
#9887=ADVANCED_FACE('',(#1521),#364,.T.);
#9962=CLOSED_SHELL('',(#9856,#9857,#9858,#9859,#9860,#9861,#9862,#9863,
#9864,#9865,#9866,#9867,#9868,#9869,#9870,#9871,#9872,#9873,#9874,#9875,
#9876,#9877,#9878,#9879,#9880,#9881,#9882,#9883,#9884,#9885,#9886,#9887));
#11059=AXIS2_PLACEMENT_3D('',#31158,#13456,#13457);
#11060=AXIS2_PLACEMENT_3D('',#31159,#13458,#13459);
#11061=AXIS2_PLACEMENT_3D('',#31161,#13460,#13461);
#11062=AXIS2_PLACEMENT_3D('',#31163,#13462,#13463);
#11063=AXIS2_PLACEMENT_3D('',#31164,#13464,#13465);
#11064=AXIS2_PLACEMENT_3D('',#31166,#13466,#13467);
#11065=AXIS2_PLACEMENT_3D('',#31215,#13492,#13493);
#11066=AXIS2_PLACEMENT_3D('',#31221,#13497,#13498);
#11067=AXIS2_PLACEMENT_3D('',#31227,#13502,#13503);
#11068=AXIS2_PLACEMENT_3D('',#31233,#13507,#13508);
#11069=AXIS2_PLACEMENT_3D('',#31239,#13512,#13513);
#11070=AXIS2_PLACEMENT_3D('',#31243,#13516,#13517);
#11071=AXIS2_PLACEMENT_3D('',#31249,#13521,#13522);
#11072=AXIS2_PLACEMENT_3D('',#31252,#13523,#13524);
#11073=AXIS2_PLACEMENT_3D('',#31253,#13525,#13526);
#11074=AXIS2_PLACEMENT_3D('',#31255,#13528,#13529);
#11075=AXIS2_PLACEMENT_3D('',#31258,#13530,#13531);
#11076=AXIS2_PLACEMENT_3D('',#31259,#13532,#13533);
#11077=AXIS2_PLACEMENT_3D('',#31262,#13535,#13536);
#11078=AXIS2_PLACEMENT_3D('',#31263,#13537,#13538);
#11079=AXIS2_PLACEMENT_3D('',#31296,#13557,#13558);
#11080=AXIS2_PLACEMENT_3D('',#31297,#13559,#13560);
#11081=AXIS2_PLACEMENT_3D('',#31299,#13562,#13563);
#11082=AXIS2_PLACEMENT_3D('',#31301,#13565,#13566);
#11083=AXIS2_PLACEMENT_3D('',#31304,#13569,#13570);
#11084=AXIS2_PLACEMENT_3D('',#31306,#13572,#13573);
#11085=AXIS2_PLACEMENT_3D('',#31308,#13575,#13576);
#11086=AXIS2_PLACEMENT_3D('',#31310,#13578,#13579);
#11087=AXIS2_PLACEMENT_3D('',#31312,#13581,#13582);
#11088=AXIS2_PLACEMENT_3D('',#31313,#13583,#13584);
#11089=AXIS2_PLACEMENT_3D('',#31315,#13586,#13587);
#11090=AXIS2_PLACEMENT_3D('',#31316,#13588,#13589);
#11091=AXIS2_PLACEMENT_3D('',#31318,#13591,#13592);
#11092=AXIS2_PLACEMENT_3D('',#31319,#13593,#13594);
#11093=AXIS2_PLACEMENT_3D('',#31321,#13596,#13597);
#11094=AXIS2_PLACEMENT_3D('',#31322,#13598,#13599);
#11095=AXIS2_PLACEMENT_3D('',#31324,#13601,#13602);
#11096=AXIS2_PLACEMENT_3D('',#31325,#13603,#13604);
#11097=AXIS2_PLACEMENT_3D('',#31327,#13606,#13607);
#11098=AXIS2_PLACEMENT_3D('',#31328,#13608,#13609);
#11099=AXIS2_PLACEMENT_3D('',#31330,#13611,#13612);
#11100=AXIS2_PLACEMENT_3D('',#31331,#13613,#13614);
#11101=AXIS2_PLACEMENT_3D('',#31332,#13615,#13616);
#13456=DIRECTION('axis',(0.,0.,1.));
#13457=DIRECTION('refdir',(1.,0.,0.));
#13458=DIRECTION('center_axis',(0.,0.,1.));
#13459=DIRECTION('ref_axis',(1.,0.,0.));
#13460=DIRECTION('center_axis',(0.,0.,1.));
#13461=DIRECTION('ref_axis',(1.,0.,0.));
#13462=DIRECTION('center_axis',(0.,0.,-1.));
#13463=DIRECTION('ref_axis',(-1.,0.,0.));
#13464=DIRECTION('center_axis',(0.,0.,-1.));
#13465=DIRECTION('ref_axis',(-1.,0.,0.));
#13466=DIRECTION('center_axis',(0.,0.,1.));
#13467=DIRECTION('ref_axis',(-1.,0.,0.));
#13468=DIRECTION('',(-0.866025403784438,-0.5,0.));
#13469=DIRECTION('',(-0.5,-0.866025403784438,0.));
#13470=DIRECTION('',(-1.,1.1556266144132E-16,0.));
#13471=DIRECTION('',(-0.866025403784438,-0.5,0.));
#13472=DIRECTION('',(-0.866025403784438,0.5,0.));
#13473=DIRECTION('',(-1.,1.1556266144132E-16,0.));
#13474=DIRECTION('',(-0.5,0.866025403784438,0.));
#13475=DIRECTION('',(-0.866025403784438,0.5,0.));
#13476=DIRECTION('',(-1.1556266144132E-16,1.,0.));
#13477=DIRECTION('',(-0.5,0.866025403784438,0.));
#13478=DIRECTION('',(0.5,0.866025403784439,0.));
#13479=DIRECTION('',(-1.1556266144132E-16,1.,0.));
#13480=DIRECTION('',(0.866025403784438,0.5,0.));
#13481=DIRECTION('',(0.5,0.866025403784438,0.));
#13482=DIRECTION('',(1.,1.1556266144132E-16,0.));
#13483=DIRECTION('',(0.866025403784438,0.5,0.));
#13484=DIRECTION('',(0.866025403784438,-0.5,0.));
#13485=DIRECTION('',(1.,1.1556266144132E-16,0.));
#13486=DIRECTION('',(0.5,-0.866025403784438,0.));
#13487=DIRECTION('',(0.866025403784438,-0.5,0.));
#13488=DIRECTION('',(0.,-1.,0.));
#13489=DIRECTION('',(0.5,-0.866025403784438,0.));
#13490=DIRECTION('',(-0.5,-0.866025403784438,0.));
#13491=DIRECTION('',(0.,-1.,0.));
#13492=DIRECTION('center_axis',(0.866025403784439,-0.5,0.));
#13493=DIRECTION('ref_axis',(0.5,0.866025403784439,0.));
#13494=DIRECTION('',(0.5,0.866025403784439,0.));
#13495=DIRECTION('',(0.,0.,1.));
#13496=DIRECTION('',(0.,0.,1.));
#13497=DIRECTION('center_axis',(1.1556266144132E-16,-1.,0.));
#13498=DIRECTION('ref_axis',(1.,1.1556266144132E-16,0.));
#13499=DIRECTION('',(1.,1.1556266144132E-16,0.));
#13500=DIRECTION('',(0.,0.,1.));
#13501=DIRECTION('',(0.,0.,1.));
#13502=DIRECTION('center_axis',(-0.866025403784439,-0.5,0.));
#13503=DIRECTION('ref_axis',(0.5,-0.866025403784439,0.));
#13504=DIRECTION('',(0.5,-0.866025403784438,0.));
#13505=DIRECTION('',(0.,0.,1.));
#13506=DIRECTION('',(0.,0.,1.));
#13507=DIRECTION('center_axis',(-0.866025403784439,0.5,0.));
#13508=DIRECTION('ref_axis',(-0.5,-0.866025403784439,0.));
#13509=DIRECTION('',(0.,0.,-1.));
#13510=DIRECTION('',(-0.5,-0.866025403784438,0.));
#13511=DIRECTION('',(0.,0.,1.));
#13512=DIRECTION('center_axis',(1.1556266144132E-16,1.,0.));
#13513=DIRECTION('ref_axis',(-1.,1.1556266144132E-16,0.));
#13514=DIRECTION('',(-1.,1.1556266144132E-16,0.));
#13515=DIRECTION('',(0.,0.,1.));
#13516=DIRECTION('center_axis',(0.866025403784438,0.5,0.));
#13517=DIRECTION('ref_axis',(-0.5,0.866025403784438,0.));
#13518=DIRECTION('',(-0.5,0.866025403784438,0.));
#13519=DIRECTION('',(0.,0.,1.));
#13520=DIRECTION('',(0.,0.,1.));
#13521=DIRECTION('center_axis',(0.,0.,-1.));
#13522=DIRECTION('ref_axis',(-1.,0.,0.));
#13523=DIRECTION('center_axis',(0.,0.,1.));
#13524=DIRECTION('ref_axis',(1.,0.,0.));
#13525=DIRECTION('center_axis',(0.,0.,1.));
#13526=DIRECTION('ref_axis',(1.,0.,0.));
#13527=DIRECTION('',(0.,0.,-1.));
#13528=DIRECTION('center_axis',(0.,0.,1.));
#13529=DIRECTION('ref_axis',(1.,0.,0.));
#13530=DIRECTION('center_axis',(0.,0.,-1.));
#13531=DIRECTION('ref_axis',(-1.,0.,0.));
#13532=DIRECTION('center_axis',(0.,0.,-1.));
#13533=DIRECTION('ref_axis',(-1.,0.,0.));
#13534=DIRECTION('',(0.,0.,-1.));
#13535=DIRECTION('center_axis',(0.,0.,1.));
#13536=DIRECTION('ref_axis',(1.,0.,0.));
#13537=DIRECTION('center_axis',(0.,0.,1.));
#13538=DIRECTION('ref_axis',(1.,0.,0.));
#13539=DIRECTION('',(0.5,-0.866025403784438,0.));
#13540=DIRECTION('',(0.,-1.,0.));
#13541=DIRECTION('',(0.866025403784438,-0.5,0.));
#13542=DIRECTION('',(1.,1.1556266144132E-16,0.));
#13543=DIRECTION('',(0.866025403784438,-0.5,0.));
#13544=DIRECTION('',(0.866025403784438,0.5,0.));
#13545=DIRECTION('',(0.5,0.866025403784439,0.));
#13546=DIRECTION('',(0.866025403784438,0.5,0.));
#13547=DIRECTION('',(-1.1556266144132E-16,1.,0.));
#13548=DIRECTION('',(-0.5,0.866025403784438,0.));
#13549=DIRECTION('',(-1.1556266144132E-16,1.,0.));
#13550=DIRECTION('',(-0.866025403784438,0.5,0.));
#13551=DIRECTION('',(-1.,1.1556266144132E-16,0.));
#13552=DIRECTION('',(-0.866025403784438,0.5,0.));
#13553=DIRECTION('',(-0.866025403784438,-0.5,0.));
#13554=DIRECTION('',(-0.866025403784438,-0.5,0.));
#13555=DIRECTION('',(0.,-1.,0.));
#13556=DIRECTION('',(-0.5,-0.866025403784438,0.));
#13557=DIRECTION('center_axis',(0.,0.,-1.));
#13558=DIRECTION('ref_axis',(1.,0.,0.));
#13559=DIRECTION('center_axis',(0.866025403784439,-0.5,0.));
#13560=DIRECTION('ref_axis',(0.5,0.866025403784439,0.));
#13561=DIRECTION('',(0.,0.,-1.));
#13562=DIRECTION('center_axis',(1.1556266144132E-16,-1.,0.));
#13563=DIRECTION('ref_axis',(1.,1.1556266144132E-16,0.));
#13564=DIRECTION('',(0.,0.,-1.));
#13565=DIRECTION('center_axis',(-0.866025403784439,-0.5,0.));
#13566=DIRECTION('ref_axis',(0.5,-0.866025403784439,0.));
#13567=DIRECTION('',(0.,0.,-1.));
#13568=DIRECTION('',(0.,0.,1.));
#13569=DIRECTION('center_axis',(-0.866025403784439,0.5,0.));
#13570=DIRECTION('ref_axis',(-0.5,-0.866025403784439,0.));
#13571=DIRECTION('',(0.,0.,1.));
#13572=DIRECTION('center_axis',(1.1556266144132E-16,1.,0.));
#13573=DIRECTION('ref_axis',(-1.,1.1556266144132E-16,0.));
#13574=DIRECTION('',(0.,0.,-1.));
#13575=DIRECTION('center_axis',(0.866025403784438,0.5,0.));
#13576=DIRECTION('ref_axis',(-0.5,0.866025403784438,0.));
#13577=DIRECTION('',(0.,0.,-1.));
#13578=DIRECTION('center_axis',(1.,1.1556266144132E-16,0.));
#13579=DIRECTION('ref_axis',(-1.1556266144132E-16,1.,0.));
#13580=DIRECTION('',(0.,0.,1.));
#13581=DIRECTION('center_axis',(0.5,0.866025403784439,0.));
#13582=DIRECTION('ref_axis',(-0.866025403784439,0.5,0.));
#13583=DIRECTION('center_axis',(0.5,0.866025403784439,0.));
#13584=DIRECTION('ref_axis',(-0.866025403784439,0.5,0.));
#13585=DIRECTION('',(0.,0.,1.));
#13586=DIRECTION('center_axis',(-0.5,0.866025403784439,0.));
#13587=DIRECTION('ref_axis',(-0.866025403784439,-0.5,0.));
#13588=DIRECTION('center_axis',(-1.,0.,0.));
#13589=DIRECTION('ref_axis',(0.,0.,1.));
#13590=DIRECTION('',(0.,0.,1.));
#13591=DIRECTION('center_axis',(-0.5,0.866025403784439,0.));
#13592=DIRECTION('ref_axis',(-0.866025403784439,-0.5,0.));
#13593=DIRECTION('center_axis',(-1.,0.,0.));
#13594=DIRECTION('ref_axis',(0.,0.,1.));
#13595=DIRECTION('',(0.,0.,1.));
#13596=DIRECTION('center_axis',(-0.5,-0.866025403784439,0.));
#13597=DIRECTION('ref_axis',(0.866025403784439,-0.5,0.));
#13598=DIRECTION('center_axis',(-0.5,-0.866025403784439,0.));
#13599=DIRECTION('ref_axis',(0.866025403784439,-0.5,0.));
#13600=DIRECTION('',(0.,0.,1.));
#13601=DIRECTION('center_axis',(0.5,-0.866025403784439,0.));
#13602=DIRECTION('ref_axis',(0.866025403784439,0.5,0.));
#13603=DIRECTION('center_axis',(0.5,-0.866025403784439,0.));
#13604=DIRECTION('ref_axis',(0.866025403784439,0.5,0.));
#13605=DIRECTION('',(0.,0.,1.));
#13606=DIRECTION('center_axis',(1.,1.1556266144132E-16,0.));
#13607=DIRECTION('ref_axis',(-1.1556266144132E-16,1.,0.));
#13608=DIRECTION('center_axis',(0.,0.,1.));
#13609=DIRECTION('ref_axis',(1.,0.,0.));
#13610=DIRECTION('',(-0.866025403784439,-1.06057523872491E-16,0.499999999999999));
#13611=DIRECTION('center_axis',(0.,0.,-1.));
#13612=DIRECTION('ref_axis',(-1.,0.,0.));
#13613=DIRECTION('center_axis',(-1.22464679914735E-16,-1.,0.));
#13614=DIRECTION('ref_axis',(1.,-1.22464679914735E-16,0.));
#13615=DIRECTION('center_axis',(0.,0.,1.));
#13616=DIRECTION('ref_axis',(1.,0.,0.));
#13617=DIRECTION('',(0.707106781186553,8.659560562355E-17,-0.707106781186542));
#31158=CARTESIAN_POINT('',(0.,0.,0.));
#31159=CARTESIAN_POINT('Origin',(0.,15.,-9.));
#31160=CARTESIAN_POINT('',(-13.8985,-1.70207535379495E-15,-9.));
#31161=CARTESIAN_POINT('Origin',(0.,0.,-9.));
#31162=CARTESIAN_POINT('',(4.5,-5.51091059616309E-16,-9.));
#31163=CARTESIAN_POINT('Origin',(0.,0.,-9.));
#31164=CARTESIAN_POINT('Origin',(0.,15.,2.44929359829471E-16));
#31165=CARTESIAN_POINT('',(14.5,-1.77573785876366E-15,2.08166817117217E-16));
#31166=CARTESIAN_POINT('Origin',(0.,0.,2.16840434497101E-16));
#31167=CARTESIAN_POINT('',(-4.7583302491977,4.7583302491977,0.));
#31168=CARTESIAN_POINT('',(-6.5,3.75277674973257,0.));
#31169=CARTESIAN_POINT('',(-3.67669907207811E-16,7.50555349946513,0.));
#31170=CARTESIAN_POINT('',(-3.75277674973257,6.5,0.));
#31171=CARTESIAN_POINT('',(-3.75277674973257,6.5,0.));
#31172=CARTESIAN_POINT('',(-1.7416697508023,6.5,0.));
#31173=CARTESIAN_POINT('',(3.75277674973257,6.5,0.));
#31174=CARTESIAN_POINT('',(-3.67669907207811E-16,7.50555349946513,0.));
#31175=CARTESIAN_POINT('',(-3.67669907207811E-16,7.50555349946513,0.));
#31176=CARTESIAN_POINT('',(1.7416697508023,6.5,0.));
#31177=CARTESIAN_POINT('',(6.5,3.75277674973257,0.));
#31178=CARTESIAN_POINT('',(3.75277674973257,6.5,0.));
#31179=CARTESIAN_POINT('',(3.75277674973257,6.5,0.));
#31180=CARTESIAN_POINT('',(4.7583302491977,4.7583302491977,0.));
#31181=CARTESIAN_POINT('',(7.50555349946514,1.02623325203886E-15,0.));
#31182=CARTESIAN_POINT('',(6.5,3.75277674973257,0.));
#31183=CARTESIAN_POINT('',(6.5,3.75277674973257,0.));
#31184=CARTESIAN_POINT('',(6.5,1.7416697508023,0.));
#31185=CARTESIAN_POINT('',(6.5,-3.75277674973257,0.));
#31186=CARTESIAN_POINT('',(7.50555349946514,0.,2.44929359829471E-16));
#31187=CARTESIAN_POINT('',(7.50555349946514,1.02623325203886E-15,0.));
#31188=CARTESIAN_POINT('',(6.5,-1.7416697508023,0.));
#31189=CARTESIAN_POINT('',(3.75277674973257,-6.5,0.));
#31190=CARTESIAN_POINT('',(6.5,-3.75277674973257,0.));
#31191=CARTESIAN_POINT('',(6.5,-3.75277674973257,0.));
#31192=CARTESIAN_POINT('',(4.7583302491977,-4.7583302491977,0.));
#31193=CARTESIAN_POINT('',(-1.19266633607575E-15,-7.50555349946513,0.));
#31194=CARTESIAN_POINT('',(3.75277674973257,-6.5,0.));
#31195=CARTESIAN_POINT('',(3.75277674973257,-6.5,0.));
#31196=CARTESIAN_POINT('',(1.7416697508023,-6.5,0.));
#31197=CARTESIAN_POINT('',(-3.75277674973256,-6.5,0.));
#31198=CARTESIAN_POINT('',(-1.19266633607575E-15,-7.50555349946513,0.));
#31199=CARTESIAN_POINT('',(-1.19266633607575E-15,-7.50555349946513,0.));
#31200=CARTESIAN_POINT('',(-1.7416697508023,-6.5,0.));
#31201=CARTESIAN_POINT('',(-6.5,-3.75277674973257,0.));
#31202=CARTESIAN_POINT('',(-3.75277674973256,-6.5,0.));
#31203=CARTESIAN_POINT('',(-3.75277674973256,-6.5,0.));
#31204=CARTESIAN_POINT('',(-4.75833024919769,-4.75833024919771,0.));
#31205=CARTESIAN_POINT('',(-7.50555349946513,1.69369577295829E-15,0.));
#31206=CARTESIAN_POINT('',(-6.5,-3.75277674973257,0.));
#31207=CARTESIAN_POINT('',(-6.5,-3.75277674973257,0.));
#31208=CARTESIAN_POINT('',(-6.5,-1.74166975080229,0.));
#31209=CARTESIAN_POINT('',(-6.5,3.75277674973257,0.));
#31210=CARTESIAN_POINT('',(-7.50555349946513,1.69369577295829E-15,0.));
#31211=CARTESIAN_POINT('',(-7.50555349946513,1.69369577295829E-15,0.));
#31212=CARTESIAN_POINT('',(-6.5,1.7416697508023,0.));
#31213=CARTESIAN_POINT('',(-3.75277674973257,6.5,0.));
#31214=CARTESIAN_POINT('',(-6.5,3.75277674973257,0.));
#31215=CARTESIAN_POINT('Origin',(3.75277674973257,-6.5,-7.));
#31216=CARTESIAN_POINT('',(6.5,-1.7416697508023,-7.));
#31217=CARTESIAN_POINT('',(7.50555349946514,1.02623325203886E-15,-7.));
#31218=CARTESIAN_POINT('',(3.75277674973257,-6.5,-7.));
#31219=CARTESIAN_POINT('',(6.5,-1.7416697508023,-7.));
#31220=CARTESIAN_POINT('',(7.50555349946514,1.02623325203886E-15,-7.));
#31221=CARTESIAN_POINT('Origin',(-3.75277674973256,-6.5,-7.));
#31222=CARTESIAN_POINT('',(1.7416697508023,-6.5,-7.));
#31223=CARTESIAN_POINT('',(3.75277674973257,-6.5,-7.));
#31224=CARTESIAN_POINT('',(-3.75277674973256,-6.5,-7.));
#31225=CARTESIAN_POINT('',(1.7416697508023,-6.5,-7.));
#31226=CARTESIAN_POINT('',(3.75277674973257,-6.5,-7.));
#31227=CARTESIAN_POINT('Origin',(-7.50555349946513,1.69369577295829E-15,
-7.));
#31228=CARTESIAN_POINT('',(-4.75833024919769,-4.75833024919771,-7.));
#31229=CARTESIAN_POINT('',(-3.75277674973256,-6.5,-7.));
#31230=CARTESIAN_POINT('',(-7.50555349946513,1.69369577295829E-15,-7.));
#31231=CARTESIAN_POINT('',(-4.7583302491977,-4.75833024919771,-7.));
#31232=CARTESIAN_POINT('',(-3.75277674973256,-6.5,-7.));
#31233=CARTESIAN_POINT('Origin',(-3.75277674973257,6.5,-7.));
#31234=CARTESIAN_POINT('',(-4.7583302491977,4.7583302491977,-7.));
#31235=CARTESIAN_POINT('',(-4.7583302491977,4.7583302491977,-7.));
#31236=CARTESIAN_POINT('',(-3.75277674973257,6.5,-7.));
#31237=CARTESIAN_POINT('',(-3.75277674973257,6.5,-7.));
#31238=CARTESIAN_POINT('',(-3.75277674973257,6.5,-7.));
#31239=CARTESIAN_POINT('Origin',(3.75277674973257,6.5,-7.));
#31240=CARTESIAN_POINT('',(-1.7416697508023,6.5,-7.));
#31241=CARTESIAN_POINT('',(3.75277674973257,6.5,-7.));
#31242=CARTESIAN_POINT('',(-1.7416697508023,6.5,-7.));
#31243=CARTESIAN_POINT('Origin',(7.50555349946514,1.02623325203886E-15,
-7.));
#31244=CARTESIAN_POINT('',(4.7583302491977,4.7583302491977,-7.));
#31245=CARTESIAN_POINT('',(3.75277674973257,6.5,-7.));
#31246=CARTESIAN_POINT('',(7.50555349946514,1.02623325203886E-15,-7.));
#31247=CARTESIAN_POINT('',(4.7583302491977,4.7583302491977,-7.));
#31248=CARTESIAN_POINT('',(3.75277674973257,6.5,-7.));
#31249=CARTESIAN_POINT('Origin',(0.,0.,0.));
#31250=CARTESIAN_POINT('',(4.5,0.,-8.15470053837925));
#31251=CARTESIAN_POINT('',(-4.5,-5.51091059616309E-16,-8.15470053837925));
#31252=CARTESIAN_POINT('Origin',(0.,0.,-8.15470053837925));
#31253=CARTESIAN_POINT('Origin',(0.,0.,-8.15470053837925));
#31254=CARTESIAN_POINT('',(4.5,-5.51091059616309E-16,0.));
#31255=CARTESIAN_POINT('Origin',(0.,0.,0.));
#31256=CARTESIAN_POINT('',(-15.,0.,-0.5));
#31257=CARTESIAN_POINT('',(15.,-1.83697019872103E-15,-0.5));
#31258=CARTESIAN_POINT('Origin',(0.,0.,-0.5));
#31259=CARTESIAN_POINT('Origin',(0.,0.,-0.5));
#31260=CARTESIAN_POINT('',(-15.,-1.83697019872103E-15,-7.89850000000002));
#31261=CARTESIAN_POINT('',(-15.,-1.83697019872103E-15,0.));
#31262=CARTESIAN_POINT('Origin',(0.,0.,-7.89850000000002));
#31263=CARTESIAN_POINT('Origin',(0.,0.,-7.));
#31264=CARTESIAN_POINT('',(-7.50555349946513,1.69369577295829E-15,-7.));
#31265=CARTESIAN_POINT('',(-6.5,-1.74166975080229,-7.));
#31266=CARTESIAN_POINT('',(-7.50555349946513,1.69369577295829E-15,-7.));
#31267=CARTESIAN_POINT('',(-6.5,-3.75277674973257,-7.));
#31268=CARTESIAN_POINT('',(-6.5,3.75277674973257,-7.));
#31269=CARTESIAN_POINT('',(-6.5,-3.75277674973257,-7.));
#31270=CARTESIAN_POINT('',(-1.7416697508023,-6.5,-7.));
#31271=CARTESIAN_POINT('',(-3.75277674973256,-6.5,-7.));
#31272=CARTESIAN_POINT('',(-1.19266633607575E-15,-7.50555349946513,-7.));
#31273=CARTESIAN_POINT('',(-6.5,-3.75277674973257,-7.));
#31274=CARTESIAN_POINT('',(-1.19266633607575E-15,-7.50555349946513,-7.));
#31275=CARTESIAN_POINT('',(4.75833024919771,-4.7583302491977,-7.));
#31276=CARTESIAN_POINT('',(3.75277674973257,-6.5,-7.));
#31277=CARTESIAN_POINT('',(6.5,-3.75277674973257,-7.));
#31278=CARTESIAN_POINT('',(-1.19266633607575E-15,-7.50555349946513,-7.));
#31279=CARTESIAN_POINT('',(6.5,-3.75277674973257,-7.));
#31280=CARTESIAN_POINT('',(6.5,1.7416697508023,-7.));
#31281=CARTESIAN_POINT('',(7.50555349946514,1.02623325203886E-15,-7.));
#31282=CARTESIAN_POINT('',(6.5,3.75277674973257,-7.));
#31283=CARTESIAN_POINT('',(6.5,-3.75277674973257,-7.));
#31284=CARTESIAN_POINT('',(6.5,3.75277674973257,-7.));
#31285=CARTESIAN_POINT('',(1.7416697508023,6.5,-7.));
#31286=CARTESIAN_POINT('',(3.75277674973257,6.5,-7.));
#31287=CARTESIAN_POINT('',(-3.67669907207811E-16,7.50555349946513,-7.));
#31288=CARTESIAN_POINT('',(6.5,3.75277674973257,-7.));
#31289=CARTESIAN_POINT('',(-3.67669907207811E-16,7.50555349946513,-7.));
#31290=CARTESIAN_POINT('',(-6.5,3.75277674973257,-7.));
#31291=CARTESIAN_POINT('',(-3.67669907207811E-16,7.50555349946513,-7.));
#31292=CARTESIAN_POINT('',(-6.5,1.7416697508023,-7.));
#31293=CARTESIAN_POINT('',(-6.5,3.75277674973257,-7.));
#31294=CARTESIAN_POINT('',(-3.75277674973257,6.5,-7.));
#31295=CARTESIAN_POINT('',(-6.50000000000001,-7.9602041944578E-16,-7.));
#31296=CARTESIAN_POINT('Origin',(0.,0.,-7.));
#31297=CARTESIAN_POINT('Origin',(3.75277674973257,-6.5,-7.));
#31298=CARTESIAN_POINT('',(4.75833024919771,-4.7583302491977,-7.));
#31299=CARTESIAN_POINT('Origin',(-3.75277674973256,-6.5,-7.));
#31300=CARTESIAN_POINT('',(-1.7416697508023,-6.5,-7.));
#31301=CARTESIAN_POINT('Origin',(-7.50555349946513,1.69369577295829E-15,
-7.));
#31302=CARTESIAN_POINT('',(-6.5,-1.74166975080229,-7.));
#31303=CARTESIAN_POINT('',(-7.50555349946513,1.69369577295829E-15,-7.));
#31304=CARTESIAN_POINT('Origin',(-3.75277674973257,6.5,-7.));
#31305=CARTESIAN_POINT('',(-6.5,1.7416697508023,-7.));
#31306=CARTESIAN_POINT('Origin',(3.75277674973257,6.5,-7.));
#31307=CARTESIAN_POINT('',(1.7416697508023,6.5,-7.));
#31308=CARTESIAN_POINT('Origin',(7.50555349946514,1.02623325203886E-15,
-7.));
#31309=CARTESIAN_POINT('',(6.5,1.7416697508023,-7.));
#31310=CARTESIAN_POINT('Origin',(6.5,-3.75277674973257,-7.));
#31311=CARTESIAN_POINT('',(6.5,3.75277674973257,-7.));
#31312=CARTESIAN_POINT('Origin',(6.5,3.75277674973257,-7.));
#31313=CARTESIAN_POINT('Origin',(6.5,3.75277674973257,-7.));
#31314=CARTESIAN_POINT('',(-3.67669907207811E-16,7.50555349946513,-7.));
#31315=CARTESIAN_POINT('Origin',(-3.67669907207811E-16,7.50555349946513,
-7.));
#31316=CARTESIAN_POINT('Origin',(-6.5,3.75277674973257,-7.));
#31317=CARTESIAN_POINT('',(-6.5,3.75277674973257,-7.));
#31318=CARTESIAN_POINT('Origin',(-3.67669907207811E-16,7.50555349946513,
-7.));
#31319=CARTESIAN_POINT('Origin',(-6.5,3.75277674973257,-7.));
#31320=CARTESIAN_POINT('',(-6.5,-3.75277674973257,-7.));
#31321=CARTESIAN_POINT('Origin',(-6.5,-3.75277674973257,-7.));
#31322=CARTESIAN_POINT('Origin',(-6.5,-3.75277674973257,-7.));
#31323=CARTESIAN_POINT('',(-1.19266633607575E-15,-7.50555349946513,-7.));
#31324=CARTESIAN_POINT('Origin',(-1.19266633607575E-15,-7.50555349946513,
-7.));
#31325=CARTESIAN_POINT('Origin',(-1.19266633607575E-15,-7.50555349946513,
-7.));
#31326=CARTESIAN_POINT('',(6.5,-3.75277674973257,-7.));
#31327=CARTESIAN_POINT('Origin',(6.5,-3.75277674973257,-7.));
#31328=CARTESIAN_POINT('Origin',(0.,0.,-7.));
#31329=CARTESIAN_POINT('',(-6.50000000000001,-7.9602041944578E-16,-7.));
#31330=CARTESIAN_POINT('Origin',(0.,0.,-0.5));
#31331=CARTESIAN_POINT('Origin',(14.5,-1.77573785876366E-15,-0.5));
#31332=CARTESIAN_POINT('Origin',(0.,0.,-9.));
#31333=CARTESIAN_POINT('',(-13.8985,-1.70207535379495E-15,-9.));
#32977=UNCERTAINTY_MEASURE_WITH_UNIT(LENGTH_MEASURE(0.01),#33017,
'DISTANCE_ACCURACY_VALUE',
'Maximum model space distance between geometric entities at asserted c
onnectivities');
#32984=UNCERTAINTY_MEASURE_WITH_UNIT(LENGTH_MEASURE(0.01),#33017,
'DISTANCE_ACCURACY_VALUE',
'Maximum model space distance between geometric entities at asserted c
onnectivities');
#33009=(
GEOMETRIC_REPRESENTATION_CONTEXT(3)
GLOBAL_UNCERTAINTY_ASSIGNED_CONTEXT((#32977))
GLOBAL_UNIT_ASSIGNED_CONTEXT((#33017,#33019,#33020))
REPRESENTATION_CONTEXT('','3D')
);
#33016=(
GEOMETRIC_REPRESENTATION_CONTEXT(3)
GLOBAL_UNCERTAINTY_ASSIGNED_CONTEXT((#32984))
GLOBAL_UNIT_ASSIGNED_CONTEXT((#33017,#33019,#33020))
REPRESENTATION_CONTEXT('','3D')
);
#33017=(
LENGTH_UNIT()
NAMED_UNIT(*)
SI_UNIT(.MILLI.,.METRE.)
);
#33019=(
NAMED_UNIT(*)
PLANE_ANGLE_UNIT()
SI_UNIT($,.RADIAN.)
);
#33020=(
NAMED_UNIT(*)
SI_UNIT($,.STERADIAN.)
SOLID_ANGLE_UNIT()
);
#33045=SHAPE_DEFINITION_REPRESENTATION(#33098,#33148);
#33098=PRODUCT_DEFINITION_SHAPE('',$,#33180);
#33148=SHAPE_REPRESENTATION('',(#11059),#33009);
#33155=PRODUCT_DEFINITION_CONTEXT('part definition',#33250,'design');
#33180=PRODUCT_DEFINITION(
'P_Torque Wrench_Handle Grip Drive_PRT-TQ-1012-11_M_Rev00',
'PRT-TQ-1012-11',#33211,#33155);
#33211=PRODUCT_DEFINITION_FORMATION('',$,#33276);
#33250=APPLICATION_CONTEXT(
'Core Data for Automotive Mechanical Design Process');
#33251=PRODUCT_CONTEXT('part definition',#33250,'mechanical');
#33276=PRODUCT(
'P_Torque Wrench_Handle Grip Drive_PRT-TQ-1012-11_M_Rev00',
'PRT-TQ-1012-11',$,(#33251));
#33288=PRESENTATION_STYLE_ASSIGNMENT((#33295));
#33295=SURFACE_STYLE_USAGE(.BOTH.,#33302);
#33302=SURFACE_SIDE_STYLE('',(#33309));
#33309=SURFACE_STYLE_FILL_AREA(#33316);
#33316=FILL_AREA_STYLE('Opaque(192,192,192)',(#33323));
#33323=FILL_AREA_STYLE_COLOUR('Opaque(192,192,192)',#33330);
#33330=COLOUR_RGB('Opaque(192,192,192)', 0.72549020, 0.75294118, 0.79215686);
ENDSEC;
END-ISO-10303-21;
